ISO-10303-21;
HEADER;
/* Generated by software containing ST-Developer
 * from STEP Tools, Inc. (www.steptools.com) 
 */

FILE_DESCRIPTION(
/* description */ ('Flywheel Crank-Slider'),
/* implementation_level */ '2;1');

FILE_NAME(
/* name */ 'Bearing bolt reducer (1).step',
/* time_stamp */ '2026-10-28T03:23:13-07:00',
/* author */ (''),
/* organization */ (''),
/* preprocessor_version */ 'ST-DEVELOPER v20.2',
/* originating_system */ 'Autodesk Translation Framework v15.17.0.0',
/* authorisation */ '');

FILE_SCHEMA (('AUTOMOTIVE_DESIGN { 1 0 10303 214 3 1 1 }'));
ENDSEC;

DATA;
#10=MECHANICAL_DESIGN_GEOMETRIC_PRESENTATION_REPRESENTATION('',(#671),#17322);
#567=SHAPE_REPRESENTATION_RELATIONSHIP('SRR','None',#17563,#619);
#619=ADVANCED_BREP_SHAPE_REPRESENTATION('',(#732),#17267);
#671=STYLED_ITEM('',(#17938),#732);
#732=MANIFOLD_SOLID_BREP('Body1',#9049);
#825=FACE_BOUND('',#1942,.T.);
#826=FACE_BOUND('',#1944,.T.);
#1031=PLANE('',#9789);
#1032=PLANE('',#9790);
#1364=FACE_OUTER_BOUND('',#1939,.T.);
#1365=FACE_OUTER_BOUND('',#1940,.T.);
#1366=FACE_OUTER_BOUND('',#1941,.T.);
#1367=FACE_OUTER_BOUND('',#1943,.T.);
#1939=EDGE_LOOP('',(#6314,#6315,#6316,#6317));
#1940=EDGE_LOOP('',(#6318,#6319,#6320,#6321));
#1941=EDGE_LOOP('',(#6322));
#1942=EDGE_LOOP('',(#6323));
#1943=EDGE_LOOP('',(#6324));
#1944=EDGE_LOOP('',(#6325));
#2664=LINE('',#13945,#3275);
#2665=LINE('',#13951,#3276);
#3275=VECTOR('',#11078,0.425);
#3276=VECTOR('',#11085,0.645);
#3886=CIRCLE('',#9784,0.425);
#3887=CIRCLE('',#9785,0.425);
#3888=CIRCLE('',#9787,0.645);
#3889=CIRCLE('',#9788,0.645);
#4341=VERTEX_POINT('',#13942);
#4342=VERTEX_POINT('',#13944);
#4343=VERTEX_POINT('',#13948);
#4344=VERTEX_POINT('',#13950);
#5114=EDGE_CURVE('',#4341,#4341,#3886,.T.);
#5115=EDGE_CURVE('',#4341,#4342,#2664,.T.);
#5116=EDGE_CURVE('',#4342,#4342,#3887,.T.);
#5117=EDGE_CURVE('',#4343,#4343,#3888,.T.);
#5118=EDGE_CURVE('',#4343,#4344,#2665,.T.);
#5119=EDGE_CURVE('',#4344,#4344,#3889,.T.);
#6314=ORIENTED_EDGE('',*,*,#5114,.F.);
#6315=ORIENTED_EDGE('',*,*,#5115,.T.);
#6316=ORIENTED_EDGE('',*,*,#5116,.T.);
#6317=ORIENTED_EDGE('',*,*,#5115,.F.);
#6318=ORIENTED_EDGE('',*,*,#5117,.F.);
#6319=ORIENTED_EDGE('',*,*,#5118,.T.);
#6320=ORIENTED_EDGE('',*,*,#5119,.T.);
#6321=ORIENTED_EDGE('',*,*,#5118,.F.);
#6322=ORIENTED_EDGE('',*,*,#5117,.T.);
#6323=ORIENTED_EDGE('',*,*,#5114,.T.);
#6324=ORIENTED_EDGE('',*,*,#5119,.F.);
#6325=ORIENTED_EDGE('',*,*,#5116,.F.);
#8354=CYLINDRICAL_SURFACE('',#9783,0.425);
#8355=CYLINDRICAL_SURFACE('',#9786,0.645);
#8555=ADVANCED_FACE('',(#1364),#8354,.F.);
#8556=ADVANCED_FACE('',(#1365),#8355,.T.);
#8557=ADVANCED_FACE('',(#1366,#825),#1031,.T.);
#8558=ADVANCED_FACE('',(#1367,#826),#1032,.F.);
#9049=CLOSED_SHELL('',(#8555,#8556,#8557,#8558));
#9782=AXIS2_PLACEMENT_3D('',#13940,#11072,#11073);
#9783=AXIS2_PLACEMENT_3D('',#13941,#11074,#11075);
#9784=AXIS2_PLACEMENT_3D('',#13943,#11076,#11077);
#9785=AXIS2_PLACEMENT_3D('',#13946,#11079,#11080);
#9786=AXIS2_PLACEMENT_3D('',#13947,#11081,#11082);
#9787=AXIS2_PLACEMENT_3D('',#13949,#11083,#11084);
#9788=AXIS2_PLACEMENT_3D('',#13952,#11086,#11087);
#9789=AXIS2_PLACEMENT_3D('',#13953,#11088,#11089);
#9790=AXIS2_PLACEMENT_3D('',#13954,#11090,#11091);
#11072=DIRECTION('axis',(0.,0.,1.));
#11073=DIRECTION('refdir',(1.,0.,0.));
#11074=DIRECTION('center_axis',(0.,0.,1.));
#11075=DIRECTION('ref_axis',(1.,0.,0.));
#11076=DIRECTION('center_axis',(0.,0.,-1.));
#11077=DIRECTION('ref_axis',(1.,0.,0.));
#11078=DIRECTION('',(0.,0.,-1.));
#11079=DIRECTION('center_axis',(0.,0.,-1.));
#11080=DIRECTION('ref_axis',(1.,0.,0.));
#11081=DIRECTION('center_axis',(0.,0.,1.));
#11082=DIRECTION('ref_axis',(1.,0.,0.));
#11083=DIRECTION('center_axis',(0.,0.,1.));
#11084=DIRECTION('ref_axis',(1.,0.,0.));
#11085=DIRECTION('',(0.,0.,-1.));
#11086=DIRECTION('center_axis',(0.,0.,1.));
#11087=DIRECTION('ref_axis',(1.,0.,0.));
#11088=DIRECTION('center_axis',(0.,0.,1.));
#11089=DIRECTION('ref_axis',(1.,0.,0.));
#11090=DIRECTION('center_axis',(0.,0.,1.));
#11091=DIRECTION('ref_axis',(1.,0.,0.));
#13940=CARTESIAN_POINT('',(0.,0.,0.));
#13941=CARTESIAN_POINT('Origin',(4.75,-15.,6.67));
#13942=CARTESIAN_POINT('',(4.325,-15.,7.87));
#13943=CARTESIAN_POINT('Origin',(4.75,-15.,7.87));
#13944=CARTESIAN_POINT('',(4.325,-15.,6.67));
#13945=CARTESIAN_POINT('',(4.325,-15.,6.67));
#13946=CARTESIAN_POINT('Origin',(4.75,-15.,6.67));
#13947=CARTESIAN_POINT('Origin',(4.75,-15.,6.67));
#13948=CARTESIAN_POINT('',(4.105,-15.,7.87));
#13949=CARTESIAN_POINT('Origin',(4.75,-15.,7.87));
#13950=CARTESIAN_POINT('',(4.105,-15.,6.67));
#13951=CARTESIAN_POINT('',(4.105,-15.,6.67));
#13952=CARTESIAN_POINT('Origin',(4.75,-15.,6.67));
#13953=CARTESIAN_POINT('Origin',(4.75,-15.,7.87));
#13954=CARTESIAN_POINT('Origin',(4.75,-15.,6.67));
#17206=UNCERTAINTY_MEASURE_WITH_UNIT(LENGTH_MEASURE(0.001),#17323,
'DISTANCE_ACCURACY_VALUE',
'Maximum model space distance between geometric entities at asserted c
onnectivities');
#17261=UNCERTAINTY_MEASURE_WITH_UNIT(LENGTH_MEASURE(0.001),#17323,
'DISTANCE_ACCURACY_VALUE',
'Maximum model space distance between geometric entities at asserted c
onnectivities');
#17267=(
GEOMETRIC_REPRESENTATION_CONTEXT(3)
GLOBAL_UNCERTAINTY_ASSIGNED_CONTEXT((#17206))
GLOBAL_UNIT_ASSIGNED_CONTEXT((#17323,#17325,#17326))
REPRESENTATION_CONTEXT('','3D')
);
#17322=(
GEOMETRIC_REPRESENTATION_CONTEXT(3)
GLOBAL_UNCERTAINTY_ASSIGNED_CONTEXT((#17261))
GLOBAL_UNIT_ASSIGNED_CONTEXT((#17323,#17325,#17326))
REPRESENTATION_CONTEXT('','3D')
);
#17323=(
LENGTH_UNIT()
NAMED_UNIT(*)
SI_UNIT(.CENTI.,.METRE.)
);
#17325=(
NAMED_UNIT(*)
PLANE_ANGLE_UNIT()
SI_UNIT($,.RADIAN.)
);
#17326=(
NAMED_UNIT(*)
SI_UNIT($,.STERADIAN.)
SOLID_ANGLE_UNIT()
);
#17332=SHAPE_DEFINITION_REPRESENTATION(#17392,#17563);
#17392=PRODUCT_DEFINITION_SHAPE('',$,#17624);
#17563=SHAPE_REPRESENTATION('',(#9782),#17267);
#17618=PRODUCT_DEFINITION_CONTEXT('part definition',#17800,'design');
#17624=PRODUCT_DEFINITION('Bearing bolt reducer (1)',
'Bearing bolt reducer (1)',#17684,#17618);
#17684=PRODUCT_DEFINITION_FORMATION('',$,#17807);
#17800=APPLICATION_CONTEXT(
'Core Data for Automotive Mechanical Design Process');
#17801=PRODUCT_CONTEXT('part definition',#17800,'mechanical');
#17807=PRODUCT('Bearing bolt reducer (1)','Bearing bolt reducer (1)',
'Bearing bolt reducer (1)',(#17801));
#17932=COLOUR_RGB('Black',0.12,0.14,0.17);
#17933=FILL_AREA_STYLE_COLOUR('',#17932);
#17934=FILL_AREA_STYLE('',(#17933));
#17935=SURFACE_STYLE_FILL_AREA(#17934);
#17936=SURFACE_SIDE_STYLE('',(#17935));
#17937=SURFACE_STYLE_USAGE(.BOTH.,#17936);
#17938=PRESENTATION_STYLE_ASSIGNMENT((#17937));
ENDSEC;
END-ISO-10303-21;
